ISO-10303-21;
HEADER;
/* Generated by software containing ST-Developer
 * from STEP Tools, Inc. (www.steptools.com) 
 */

FILE_DESCRIPTION(
/* description */ ('STEP AP214'),
/* implementation_level */ '2;1');

FILE_NAME(
/* name */ 'PRT-TQ-1012-14.step',
/* time_stamp */ '2026-10-07T12:49:37-07:00',
/* author */ (''),
/* organization */ (''),
/* preprocessor_version */ 'ST-DEVELOPER v20.2',
/* originating_system */ 'Autodesk Translation Framework v15.15.0.0',
/* authorisation */ '');

FILE_SCHEMA (('AUTOMOTIVE_DESIGN { 1 0 10303 214 3 1 1 }'));
ENDSEC;

DATA;
#10=MECHANICAL_DESIGN_GEOMETRIC_PRESENTATION_REPRESENTATION('',(#309),#33016);
#251=SHAPE_REPRESENTATION_RELATIONSHIP('SRR','None',#33145,#278);
#278=ADVANCED_BREP_SHAPE_REPRESENTATION('',(#336),#33006);
#309=STYLED_ITEM('',(#33288),#336);
#336=MANIFOLD_SOLID_BREP('Body1',#9960);
#524=FACE_BOUND('',#2008,.T.);
#525=FACE_BOUND('',#2012,.T.);
#526=FACE_BOUND('',#2015,.T.);
#964=PLANE('',#10908);
#965=PLANE('',#10912);
#966=PLANE('',#10913);
#967=PLANE('',#10918);
#968=PLANE('',#10919);
#1400=FACE_OUTER_BOUND('',#2006,.T.);
#1401=FACE_OUTER_BOUND('',#2007,.T.);
#1402=FACE_OUTER_BOUND('',#2009,.T.);
#1403=FACE_OUTER_BOUND('',#2010,.T.);
#1404=FACE_OUTER_BOUND('',#2011,.T.);
#1405=FACE_OUTER_BOUND('',#2013,.T.);
#1406=FACE_OUTER_BOUND('',#2014,.T.);
#1407=FACE_OUTER_BOUND('',#2016,.T.);
#1408=FACE_OUTER_BOUND('',#2017,.T.);
#2006=EDGE_LOOP('',(#8318,#8319,#8320,#8321));
#2007=EDGE_LOOP('',(#8322));
#2008=EDGE_LOOP('',(#8323));
#2009=EDGE_LOOP('',(#8324,#8325,#8326,#8327));
#2010=EDGE_LOOP('',(#8328));
#2011=EDGE_LOOP('',(#8329));
#2012=EDGE_LOOP('',(#8330));
#2013=EDGE_LOOP('',(#8331,#8332,#8333,#8334));
#2014=EDGE_LOOP('',(#8335));
#2015=EDGE_LOOP('',(#8336));
#2016=EDGE_LOOP('',(#8337));
#2017=EDGE_LOOP('',(#8338,#8339,#8340,#8341));
#2468=CIRCLE('',#10906,3.);
#2469=CIRCLE('',#10907,3.);
#2470=CIRCLE('',#10909,3.75);
#2471=CIRCLE('',#10911,3.75);
#2472=CIRCLE('',#10914,3.);
#2473=CIRCLE('',#10915,2.4);
#2474=CIRCLE('',#10917,2.4);
#2475=CIRCLE('',#10920,3.);
#3180=LINE('',#28003,#3930);
#3181=LINE('',#28010,#3931);
#3182=LINE('',#28020,#3932);
#3183=LINE('',#28027,#3933);
#3930=VECTOR('',#13093,3.);
#3931=VECTOR('',#13102,3.75);
#3932=VECTOR('',#13115,2.4);
#3933=VECTOR('',#13126,3.);
#4723=VERTEX_POINT('',#28000);
#4724=VERTEX_POINT('',#28002);
#4725=VERTEX_POINT('',#28006);
#4726=VERTEX_POINT('',#28009);
#4727=VERTEX_POINT('',#28014);
#4728=VERTEX_POINT('',#28016);
#4729=VERTEX_POINT('',#28019);
#4730=VERTEX_POINT('',#28024);
#5972=EDGE_CURVE('',#4723,#4723,#2468,.T.);
#5973=EDGE_CURVE('',#4723,#4724,#3180,.T.);
#5974=EDGE_CURVE('',#4724,#4724,#2469,.T.);
#5975=EDGE_CURVE('',#4725,#4725,#2470,.T.);
#5976=EDGE_CURVE('',#4725,#4726,#3181,.T.);
#5977=EDGE_CURVE('',#4726,#4726,#2471,.T.);
#5978=EDGE_CURVE('',#4727,#4727,#2472,.T.);
#5979=EDGE_CURVE('',#4728,#4728,#2473,.T.);
#5980=EDGE_CURVE('',#4728,#4729,#3182,.T.);
#5981=EDGE_CURVE('',#4729,#4729,#2474,.T.);
#5982=EDGE_CURVE('',#4730,#4730,#2475,.T.);
#5983=EDGE_CURVE('',#4730,#4727,#3183,.T.);
#8318=ORIENTED_EDGE('',*,*,#5972,.F.);
#8319=ORIENTED_EDGE('',*,*,#5973,.T.);
#8320=ORIENTED_EDGE('',*,*,#5974,.T.);
#8321=ORIENTED_EDGE('',*,*,#5973,.F.);
#8322=ORIENTED_EDGE('',*,*,#5975,.T.);
#8323=ORIENTED_EDGE('',*,*,#5974,.F.);
#8324=ORIENTED_EDGE('',*,*,#5975,.F.);
#8325=ORIENTED_EDGE('',*,*,#5976,.T.);
#8326=ORIENTED_EDGE('',*,*,#5977,.T.);
#8327=ORIENTED_EDGE('',*,*,#5976,.F.);
#8328=ORIENTED_EDGE('',*,*,#5977,.F.);
#8329=ORIENTED_EDGE('',*,*,#5978,.F.);
#8330=ORIENTED_EDGE('',*,*,#5979,.T.);
#8331=ORIENTED_EDGE('',*,*,#5979,.F.);
#8332=ORIENTED_EDGE('',*,*,#5980,.T.);
#8333=ORIENTED_EDGE('',*,*,#5981,.T.);
#8334=ORIENTED_EDGE('',*,*,#5980,.F.);
#8335=ORIENTED_EDGE('',*,*,#5972,.T.);
#8336=ORIENTED_EDGE('',*,*,#5981,.F.);
#8337=ORIENTED_EDGE('',*,*,#5982,.T.);
#8338=ORIENTED_EDGE('',*,*,#5982,.F.);
#8339=ORIENTED_EDGE('',*,*,#5983,.T.);
#8340=ORIENTED_EDGE('',*,*,#5978,.T.);
#8341=ORIENTED_EDGE('',*,*,#5983,.F.);
#9318=CYLINDRICAL_SURFACE('',#10905,3.);
#9319=CYLINDRICAL_SURFACE('',#10910,3.75);
#9320=CYLINDRICAL_SURFACE('',#10916,2.4);
#9321=CYLINDRICAL_SURFACE('',#10921,3.);
#9766=ADVANCED_FACE('',(#1400),#9318,.T.);
#9767=ADVANCED_FACE('',(#1401,#524),#964,.F.);
#9768=ADVANCED_FACE('',(#1402),#9319,.T.);
#9769=ADVANCED_FACE('',(#1403),#965,.F.);
#9770=ADVANCED_FACE('',(#1404,#525),#966,.T.);
#9771=ADVANCED_FACE('',(#1405),#9320,.T.);
#9772=ADVANCED_FACE('',(#1406,#526),#967,.T.);
#9773=ADVANCED_FACE('',(#1407),#968,.F.);
#9774=ADVANCED_FACE('',(#1408),#9321,.T.);
#9960=CLOSED_SHELL('',(#9766,#9767,#9768,#9769,#9770,#9771,#9772,#9773,
#9774));
#10904=AXIS2_PLACEMENT_3D('',#27998,#13087,#13088);
#10905=AXIS2_PLACEMENT_3D('',#27999,#13089,#13090);
#10906=AXIS2_PLACEMENT_3D('',#28001,#13091,#13092);
#10907=AXIS2_PLACEMENT_3D('',#28004,#13094,#13095);
#10908=AXIS2_PLACEMENT_3D('',#28005,#13096,#13097);
#10909=AXIS2_PLACEMENT_3D('',#28007,#13098,#13099);
#10910=AXIS2_PLACEMENT_3D('',#28008,#13100,#13101);
#10911=AXIS2_PLACEMENT_3D('',#28011,#13103,#13104);
#10912=AXIS2_PLACEMENT_3D('',#28012,#13105,#13106);
#10913=AXIS2_PLACEMENT_3D('',#28013,#13107,#13108);
#10914=AXIS2_PLACEMENT_3D('',#28015,#13109,#13110);
#10915=AXIS2_PLACEMENT_3D('',#28017,#13111,#13112);
#10916=AXIS2_PLACEMENT_3D('',#28018,#13113,#13114);
#10917=AXIS2_PLACEMENT_3D('',#28021,#13116,#13117);
#10918=AXIS2_PLACEMENT_3D('',#28022,#13118,#13119);
#10919=AXIS2_PLACEMENT_3D('',#28023,#13120,#13121);
#10920=AXIS2_PLACEMENT_3D('',#28025,#13122,#13123);
#10921=AXIS2_PLACEMENT_3D('',#28026,#13124,#13125);
#13087=DIRECTION('axis',(0.,0.,1.));
#13088=DIRECTION('refdir',(1.,0.,0.));
#13089=DIRECTION('center_axis',(0.,-1.,0.));
#13090=DIRECTION('ref_axis',(0.,0.,-1.));
#13091=DIRECTION('center_axis',(0.,-1.,0.));
#13092=DIRECTION('ref_axis',(0.,0.,-1.));
#13093=DIRECTION('',(0.,1.,0.));
#13094=DIRECTION('center_axis',(0.,-1.,0.));
#13095=DIRECTION('ref_axis',(0.,0.,-1.));
#13096=DIRECTION('center_axis',(0.,1.,0.));
#13097=DIRECTION('ref_axis',(0.,0.,1.));
#13098=DIRECTION('center_axis',(0.,-1.,0.));
#13099=DIRECTION('ref_axis',(0.,0.,-1.));
#13100=DIRECTION('center_axis',(0.,-1.,0.));
#13101=DIRECTION('ref_axis',(0.,0.,-1.));
#13102=DIRECTION('',(0.,1.,0.));
#13103=DIRECTION('center_axis',(0.,-1.,0.));
#13104=DIRECTION('ref_axis',(0.,0.,-1.));
#13105=DIRECTION('center_axis',(0.,-1.,0.));
#13106=DIRECTION('ref_axis',(0.,0.,-1.));
#13107=DIRECTION('center_axis',(0.,1.,0.));
#13108=DIRECTION('ref_axis',(0.,0.,1.));
#13109=DIRECTION('center_axis',(0.,-1.,0.));
#13110=DIRECTION('ref_axis',(0.,0.,-1.));
#13111=DIRECTION('center_axis',(0.,-1.,0.));
#13112=DIRECTION('ref_axis',(0.,0.,-1.));
#13113=DIRECTION('center_axis',(0.,-1.,0.));
#13114=DIRECTION('ref_axis',(0.,0.,-1.));
#13115=DIRECTION('',(0.,1.,0.));
#13116=DIRECTION('center_axis',(0.,-1.,0.));
#13117=DIRECTION('ref_axis',(0.,0.,-1.));
#13118=DIRECTION('center_axis',(0.,-1.,0.));
#13119=DIRECTION('ref_axis',(0.,0.,-1.));
#13120=DIRECTION('center_axis',(0.,1.,0.));
#13121=DIRECTION('ref_axis',(0.,0.,1.));
#13122=DIRECTION('center_axis',(0.,-1.,0.));
#13123=DIRECTION('ref_axis',(0.,0.,-1.));
#13124=DIRECTION('center_axis',(0.,-1.,0.));
#13125=DIRECTION('ref_axis',(0.,0.,-1.));
#13126=DIRECTION('',(0.,1.,0.));
#27998=CARTESIAN_POINT('',(0.,0.,0.));
#27999=CARTESIAN_POINT('Origin',(0.,0.,0.));
#28000=CARTESIAN_POINT('',(-3.67394039744206E-16,2.1,3.));
#28001=CARTESIAN_POINT('Origin',(0.,2.1,0.));
#28002=CARTESIAN_POINT('',(-3.67394039744206E-16,25.,3.));
#28003=CARTESIAN_POINT('',(-3.67394039744206E-16,0.,3.));
#28004=CARTESIAN_POINT('Origin',(0.,25.,0.));
#28005=CARTESIAN_POINT('Origin',(-3.75,25.,0.));
#28006=CARTESIAN_POINT('',(-4.59242549680257E-16,25.,3.75));
#28007=CARTESIAN_POINT('Origin',(0.,25.,0.));
#28008=CARTESIAN_POINT('Origin',(0.,0.,0.));
#28009=CARTESIAN_POINT('',(-4.59242549680257E-16,26.,3.75));
#28010=CARTESIAN_POINT('',(-4.59242549680257E-16,0.,3.75));
#28011=CARTESIAN_POINT('Origin',(0.,26.,0.));
#28012=CARTESIAN_POINT('Origin',(0.,26.,0.));
#28013=CARTESIAN_POINT('Origin',(-3.,1.1,0.));
#28014=CARTESIAN_POINT('',(-3.67394039744206E-16,1.1,3.));
#28015=CARTESIAN_POINT('Origin',(0.,1.1,0.));
#28016=CARTESIAN_POINT('',(-2.93915231795365E-16,1.1,2.4));
#28017=CARTESIAN_POINT('Origin',(0.,1.1,0.));
#28018=CARTESIAN_POINT('Origin',(0.,0.,0.));
#28019=CARTESIAN_POINT('',(-2.93915231795365E-16,2.1,2.4));
#28020=CARTESIAN_POINT('',(-2.93915231795365E-16,0.,2.4));
#28021=CARTESIAN_POINT('Origin',(0.,2.1,0.));
#28022=CARTESIAN_POINT('Origin',(-3.,2.1,0.));
#28023=CARTESIAN_POINT('Origin',(0.,0.,0.));
#28024=CARTESIAN_POINT('',(-3.67394039744206E-16,0.,3.));
#28025=CARTESIAN_POINT('Origin',(0.,0.,0.));
#28026=CARTESIAN_POINT('Origin',(0.,0.,0.));
#28027=CARTESIAN_POINT('',(-3.67394039744206E-16,0.,3.));
#32974=UNCERTAINTY_MEASURE_WITH_UNIT(LENGTH_MEASURE(0.01),#33017,
'DISTANCE_ACCURACY_VALUE',
'Maximum model space distance between geometric entities at asserted c
onnectivities');
#32984=UNCERTAINTY_MEASURE_WITH_UNIT(LENGTH_MEASURE(0.01),#33017,
'DISTANCE_ACCURACY_VALUE',
'Maximum model space distance between geometric entities at asserted c
onnectivities');
#33006=(
GEOMETRIC_REPRESENTATION_CONTEXT(3)
GLOBAL_UNCERTAINTY_ASSIGNED_CONTEXT((#32974))
GLOBAL_UNIT_ASSIGNED_CONTEXT((#33017,#33019,#33020))
REPRESENTATION_CONTEXT('','3D')
);
#33016=(
GEOMETRIC_REPRESENTATION_CONTEXT(3)
GLOBAL_UNCERTAINTY_ASSIGNED_CONTEXT((#32984))
GLOBAL_UNIT_ASSIGNED_CONTEXT((#33017,#33019,#33020))
REPRESENTATION_CONTEXT('','3D')
);
#33017=(
LENGTH_UNIT()
NAMED_UNIT(*)
SI_UNIT(.MILLI.,.METRE.)
);
#33019=(
NAMED_UNIT(*)
PLANE_ANGLE_UNIT()
SI_UNIT($,.RADIAN.)
);
#33020=(
NAMED_UNIT(*)
SI_UNIT($,.STERADIAN.)
SOLID_ANGLE_UNIT()
);
#33042=SHAPE_DEFINITION_REPRESENTATION(#33095,#33145);
#33095=PRODUCT_DEFINITION_SHAPE('',$,#33177);
#33145=SHAPE_REPRESENTATION('',(#10904),#33006);
#33155=PRODUCT_DEFINITION_CONTEXT('part definition',#33250,'design');
#33177=PRODUCT_DEFINITION(
'P_Torque Wrench_Head Handle Lock Pin_PRT-TQ-1012-14_M_Rev00',
'PRT-TQ-1012-14',#33208,#33155);
#33208=PRODUCT_DEFINITION_FORMATION('',$,#33273);
#33250=APPLICATION_CONTEXT(
'Core Data for Automotive Mechanical Design Process');
#33251=PRODUCT_CONTEXT('part definition',#33250,'mechanical');
#33273=PRODUCT(
'P_Torque Wrench_Head Handle Lock Pin_PRT-TQ-1012-14_M_Rev00',
'PRT-TQ-1012-14',$,(#33251));
#33288=PRESENTATION_STYLE_ASSIGNMENT((#33295));
#33295=SURFACE_STYLE_USAGE(.BOTH.,#33302);
#33302=SURFACE_SIDE_STYLE('',(#33309));
#33309=SURFACE_STYLE_FILL_AREA(#33316);
#33316=FILL_AREA_STYLE('Opaque(192,192,192)',(#33323));
#33323=FILL_AREA_STYLE_COLOUR('Opaque(192,192,192)',#33330);
#33330=COLOUR_RGB('Opaque(192,192,192)', 0.72549020, 0.75294118, 0.79215686);
ENDSEC;
END-ISO-10303-21;
